ISO-10303-21;
HEADER;
FILE_DESCRIPTION (('STEP AP214'),
    '1' );
FILE_NAME ('socket head cap screw_iso_ISO 4762 M5 x 16 - 16N.step',
    '2026-10-08T13:46:47',
    ( '' ),
    ( '' ),
    'SwSTEP 2.0',
    'SolidWorks 2026',
    '' );
FILE_SCHEMA (( 'AUTOMOTIVE_DESIGN' ));
ENDSEC;

DATA;
#92=DIRECTION ( 'NONE',  ( 0.000000000000000000, 0.000000000000000000, -1.000000000000000000 ) ) ;
#157=DIRECTION ( 'NONE',  ( 0.000000000000000000, -0.5000000000000013323, -0.8660254037844380415 ) ) ;
#182=CARTESIAN_POINT ( 'NONE',  ( 2.500000000000000000, -1.178949249685214307, 2.042000000000001592 ) ) ;
#219=CARTESIAN_POINT ( 'NONE',  ( 5.000000000000002665, 3.306546357697854226E-16, 2.700000000000000622 ) ) ;
#269=CARTESIAN_POINT ( 'NONE',  ( 5.200000000000002842, 0.000000000000000000, 0.000000000000000000 ) ) ;
#309=FILL_AREA_STYLE ('',( #2348 ) ) ;
#336=AXIS2_PLACEMENT_3D ( 'NONE', #17862, #16313, #17643 ) ;
#428=VERTEX_POINT ( 'NONE', #15531 ) ;
#434=SURFACE_STYLE_FILL_AREA ( #309 ) ;
#473=DIRECTION ( 'NONE',  ( 0.000000000000000000, 1.224646799147353207E-16, 1.000000000000000000 ) ) ;
#479=EDGE_CURVE ( 'NONE', #2500, #428, #11820, .T. ) ;
#529=FACE_OUTER_BOUND ( 'NONE', #22717, .T. ) ;
#577=ORIENTED_EDGE ( 'NONE', *, *, #10412, .F. ) ;
#611=VERTEX_POINT ( 'NONE', #2056 ) ;
#695=ORIENTED_EDGE ( 'NONE', *, *, #8510, .F. ) ;
#759=( NAMED_UNIT ( * ) SI_UNIT ( $, .STERADIAN. ) SOLID_ANGLE_UNIT ( ) );
#765=VECTOR ( 'NONE', #19219, 1000.000000000000114 ) ;
#777=AXIS2_PLACEMENT_3D ( 'NONE', #21806, #19998, #1567 ) ;
#804=CIRCLE ( 'NONE', #6927, 4.250000000000000000 ) ;
#808=CARTESIAN_POINT ( 'NONE',  ( 0.000000000000000000, 2.357898499370431722, -2.818925648462311528E-15 ) ) ;
#908=PRODUCT ( 'socket head cap screw_iso_ISO 4762 M5 x 16 - 16N', 'socket head cap screw_iso_ISO 4762 M5 x 16 - 16N', '', ( #6130 ) ) ;
#910=CARTESIAN_POINT ( 'NONE',  ( 2.500000000000000000, 2.357898499370431722, -2.818925648462311528E-15 ) ) ;
#948=LINE ( 'NONE', #12006, #2112 ) ;
#975=LINE ( 'NONE', #6510, #11280 ) ;
#995=CARTESIAN_POINT ( 'NONE',  ( 2.500000000000000000, -2.357898499370432166, 3.035766082959412415E-15 ) ) ;
#1027=PLANE ( 'NONE',  #22161 ) ;
#1153=ORIENTED_EDGE ( 'NONE', *, *, #22526, .T. ) ;
#1182=DIRECTION ( 'NONE',  ( -1.000000000000000000, -0.000000000000000000, -0.000000000000000000 ) ) ;
#1184=ORIENTED_EDGE ( 'NONE', *, *, #8510, .T. ) ;
#1245=ORIENTED_EDGE ( 'NONE', *, *, #12789, .T. ) ;
#1248=ORIENTED_EDGE ( 'NONE', *, *, #5366, .T. ) ;
#1285=ADVANCED_FACE ( 'NONE', ( #3744 ), #7930, .F. ) ;
#1291=DIRECTION ( 'NONE',  ( 1.000000000000000000, 0.000000000000000000, 0.000000000000000000 ) ) ;
#1314=VECTOR ( 'NONE', #157, 999.9999999999997726 ) ;
#1317=CYLINDRICAL_SURFACE ( 'NONE', #10700, 4.250000000000000000 ) ;
#1343=DIRECTION ( 'NONE',  ( 0.000000000000000000, 0.000000000000000000, -1.000000000000000000 ) ) ;
#1456=ORIENTED_EDGE ( 'NONE', *, *, #8400, .F. ) ;
#1458=ORIENTED_EDGE ( 'NONE', *, *, #22694, .F. ) ;
#1506=CIRCLE ( 'NONE', #5720, 2.500000000000000888 ) ;
#1545=FACE_OUTER_BOUND ( 'NONE', #5338, .T. ) ;
#1567=DIRECTION ( 'NONE',  ( 0.000000000000000000, 0.000000000000000000, 1.000000000000000000 ) ) ;
#1586=CARTESIAN_POINT ( 'NONE',  ( 21.00000000000000355, 0.000000000000000000, 0.000000000000000000 ) ) ;
#1608=DIRECTION ( 'NONE',  ( 1.000000000000000000, 0.000000000000000000, 0.000000000000000000 ) ) ;
#1610=ADVANCED_FACE ( 'NONE', ( #19439 ), #4963, .F. ) ;
#1684=DIRECTION ( 'NONE',  ( -0.5000000000000051070, 0.000000000000000000, 0.8660254037844355990 ) ) ;
#1704=DIRECTION ( 'NONE',  ( 1.000000000000000000, 0.000000000000000000, 0.000000000000000000 ) ) ;
#1724=ORIENTED_EDGE ( 'NONE', *, *, #5716, .F. ) ;
#1761=ADVANCED_FACE ( 'NONE', ( #5907 ), #2582, .T. ) ;
#1775=FACE_OUTER_BOUND ( 'NONE', #22420, .T. ) ;
#1778=CARTESIAN_POINT ( 'NONE',  ( 0.2500000000000002220, 0.000000000000000000, 4.000000000000000000 ) ) ;
#1812=ORIENTED_EDGE ( 'NONE', *, *, #19152, .F. ) ;
#1847=CIRCLE ( 'NONE', #13414, 4.250000000000000000 ) ;
#1883=ADVANCED_BREP_SHAPE_REPRESENTATION ( '', ( #6242, #7318 ), #5664 ) ;
#1902=ORIENTED_EDGE ( 'NONE', *, *, #11855, .T. ) ;
#1908=CARTESIAN_POINT ( 'NONE',  ( 2.500000000000000000, -1.178949249685214307, 2.042000000000001592 ) ) ;
#1923=CARTESIAN_POINT ( 'NONE',  ( 2.500000000000000000, 1.178949249685212974, -2.042000000000001148 ) ) ;
#1966=EDGE_CURVE ( 'NONE', #6314, #9649, #2882, .T. ) ;
#2051=EDGE_CURVE ( 'NONE', #12043, #8977, #6382, .T. ) ;
#2056=CARTESIAN_POINT ( 'NONE',  ( 2.500000000000000000, 2.357898499370431722, -2.818925648462311528E-15 ) ) ;
#2059=AXIS2_PLACEMENT_3D ( 'NONE', #10357, #21086, #8435 ) ;
#2075=DIRECTION ( 'NONE',  ( 0.000000000000000000, 0.000000000000000000, -1.000000000000000000 ) ) ;
#2083=DIRECTION ( 'NONE',  ( 0.000000000000000000, -0.5000000000000009992, -0.8660254037844380415 ) ) ;
#2085=CIRCLE ( 'NONE', #10157, 2.055000000000000160 ) ;
#2112=VECTOR ( 'NONE', #22635, 1000.000000000000000 ) ;
#2137=DIRECTION ( 'NONE',  ( -0.000000000000000000, 1.287488025362403787E-15, 1.000000000000000000 ) ) ;
#2167=CIRCLE ( 'NONE', #15972, 4.000000000000000000 ) ;
#2183=( GEOMETRIC_REPRESENTATION_CONTEXT ( 3 ) GLOBAL_UNCERTAINTY_ASSIGNED_CONTEXT ( ( #11496 ) ) GLOBAL_UNIT_ASSIGNED_CONTEXT ( ( #16970, #18636, #7870 ) ) REPRESENTATION_CONTEXT ( 'NONE', 'WORKASPACE' ) );
#2184=AXIS2_PLACEMENT_3D ( 'NONE', #13301, #20569, #13654 ) ;
#2188=ORIENTED_EDGE ( 'NONE', *, *, #19977, .F. ) ;
#2190=( NAMED_UNIT ( * ) SI_UNIT ( $, .STERADIAN. ) SOLID_ANGLE_UNIT ( ) );
#2211=CARTESIAN_POINT ( 'NONE',  ( 21.00000000000000355, 0.000000000000000000, 2.055000000000000160 ) ) ;
#2220=CIRCLE ( 'NONE', #5290, 2.041999999999999815 ) ;
#2252=CARTESIAN_POINT ( 'NONE',  ( -31.74999999999995737, 0.000000000000000000, 0.000000000000000000 ) ) ;
#2254=CARTESIAN_POINT ( 'NONE',  ( 5.200000000000002842, 0.000000000000000000, 2.500000000000000444 ) ) ;
#2303=DIRECTION ( 'NONE',  ( 0.000000000000000000, 1.000000000000000000, -1.287488025362403787E-15 ) ) ;
#2313=AXIS2_PLACEMENT_3D ( 'NONE', #21472, #23163, #23405 ) ;
#2328=VECTOR ( 'NONE', #5880, 1000.000000000000114 ) ;
#2347=ORIENTED_EDGE ( 'NONE', *, *, #6296, .T. ) ;
#2348=FILL_AREA_STYLE_COLOUR ( '', #21300 ) ;
#2350=ORIENTED_EDGE ( 'NONE', *, *, #22694, .T. ) ;
#2358=CARTESIAN_POINT ( 'NONE',  ( 21.00000000000000355, 2.789133085058097101E-16, -2.055000000000000160 ) ) ;
#2424=ORIENTED_EDGE ( 'NONE', *, *, #479, .T. ) ;
#2425=CARTESIAN_POINT ( 'NONE',  ( 4.999999999999997335, 0.000000000000000000, 4.250000000000000000 ) ) ;
#2459=ORIENTED_EDGE ( 'NONE', *, *, #13057, .T. ) ;
#2471=DIRECTION ( 'NONE',  ( -1.000000000000000000, -0.000000000000000000, -0.000000000000000000 ) ) ;
#2500=VERTEX_POINT ( 'NONE', #14024 ) ;
#2508=DIRECTION ( 'NONE',  ( -0.000000000000000000, 0.000000000000000000, 1.000000000000000000 ) ) ;
#2514=VECTOR ( 'NONE', #14476, 1000.000000000000000 ) ;
#2545=DIRECTION ( 'NONE',  ( 0.000000000000000000, 0.000000000000000000, 1.000000000000000000 ) ) ;
#2555=AXIS2_PLACEMENT_3D ( 'NONE', #23498, #20011, #9160 ) ;
#2570=APPLICATION_CONTEXT ( 'automotive_design' ) ;
#2576=ORIENTED_EDGE ( 'NONE', *, *, #16881, .T. ) ;
#2582=CONICAL_SURFACE ( 'NONE', #22482, 2.055000000000000160, 0.7853981633974639331 ) ;
#2608=ORIENTED_EDGE ( 'NONE', *, *, #4965, .F. ) ;
#2613=VECTOR ( 'NONE', #6455, 1000.000000000000000 ) ;
#2640=ADVANCED_FACE ( 'NONE', ( #1775 ), #23078, .T. ) ;
#2749=CARTESIAN_POINT ( 'NONE',  ( 2.500000000000000000, -2.357898499370432166, 3.035766082959412415E-15 ) ) ;
#2781=( NAMED_UNIT ( * ) PLANE_ANGLE_UNIT ( ) SI_UNIT ( $, .RADIAN. ) );
#2794=PLANE ( 'NONE',  #19024 ) ;
#2850=ORIENTED_EDGE ( 'NONE', *, *, #23330, .F. ) ;
#2882=LINE ( 'NONE', #15502, #21512 ) ;
#2887=DIRECTION ( 'NONE',  ( 0.000000000000000000, -1.000000000000000000, 1.287488025362403787E-15 ) ) ;
#2896=EDGE_CURVE ( 'NONE', #16753, #13902, #17692, .T. ) ;
#3002=LINE ( 'NONE', #23479, #20974 ) ;
#3006=DIRECTION ( 'NONE',  ( -1.000000000000000000, -0.000000000000000000, -0.000000000000000000 ) ) ;
#3019=LINE ( 'NONE', #23137, #19415 ) ;
#3050=FACE_OUTER_BOUND ( 'NONE', #6832, .T. ) ;
#3111=CARTESIAN_POINT ( 'NONE',  ( 0.000000000000000000, 0.000000000000000000, 0.000000000000000000 ) ) ;
#3211=CARTESIAN_POINT ( 'NONE',  ( 2.500000000000000000, 2.357898499370431722, -2.818925648462311528E-15 ) ) ;
#3251=LINE ( 'NONE', #16201, #11133 ) ;
#3272=DIRECTION ( 'NONE',  ( 0.000000000000000000, 0.000000000000000000, 1.000000000000000000 ) ) ;
#3298=ORIENTED_EDGE ( 'NONE', *, *, #23598, .T. ) ;
#3375=TOROIDAL_SURFACE ( 'NONE', #3739, 4.000000000000000000, 0.2500000000000000000 ) ;
#3400=DIRECTION ( 'NONE',  ( 0.000000000000000000, 0.000000000000000000, 1.000000000000000000 ) ) ;
#3402=AXIS2_PLACEMENT_3D ( 'NONE', #3211, #17832, #15591 ) ;
#3437=DIRECTION ( 'NONE',  ( -1.000000000000000000, -0.000000000000000000, -0.000000000000000000 ) ) ;
#3473=ORIENTED_EDGE ( 'NONE', *, *, #22648, .T. ) ;
#3549=LINE ( 'NONE', #5228, #2514 ) ;
#3556=CARTESIAN_POINT ( 'NONE',  ( 2.500000000000000000, 2.500728763858895382E-16, -2.041999999999999815 ) ) ;
#3630=VERTEX_POINT ( 'NONE', #219 ) ;
#3635=EDGE_CURVE ( 'NONE', #19193, #23445, #5976, .T. ) ;
#3636=CYLINDRICAL_SURFACE ( 'NONE', #12079, 2.500000000000000444 ) ;
#3698=AXIS2_PLACEMENT_3D ( 'NONE', #5075, #1704, #12297 ) ;
#3739=AXIS2_PLACEMENT_3D ( 'NONE', #4245, #19201, #2545 ) ;
#3744=FACE_OUTER_BOUND ( 'NONE', #20065, .T. ) ;
#3745=DIRECTION ( 'NONE',  ( 0.000000000000000000, -0.4999999999999993339, 0.8660254037844390407 ) ) ;
#3786=VECTOR ( 'NONE', #8893, 1000.000000000000000 ) ;
#3834=AXIS2_PLACEMENT_3D ( 'NONE', #11641, #2137, #13307 ) ;
#3872=DIRECTION ( 'NONE',  ( 1.000000000000000000, 0.000000000000000000, 0.000000000000000000 ) ) ;
#3882=FACE_OUTER_BOUND ( 'NONE', #22931, .T. ) ;
#3910=DIRECTION ( 'NONE',  ( 0.000000000000000000, 0.000000000000000000, 1.000000000000000000 ) ) ;
#3935=ORIENTED_EDGE ( 'NONE', *, *, #10441, .F. ) ;
#3937=ORIENTED_EDGE ( 'NONE', *, *, #16094, .F. ) ;
#4040=CIRCLE ( 'NONE', #9416, 4.000000000000000000 ) ;
#4058=ORIENTED_EDGE ( 'NONE', *, *, #22648, .F. ) ;
#4063=CARTESIAN_POINT ( 'NONE',  ( -31.74999999999995737, 3.061616997868383634E-16, -2.500000000000000444 ) ) ;
#4069=EDGE_LOOP ( 'NONE', ( #16529, #16721, #18086 ) ) ;
#4126=ADVANCED_FACE ( 'NONE', ( #20316, #11256 ), #11375, .T. ) ;
#4210=SHAPE_DEFINITION_REPRESENTATION ( #20786, #6707 ) ;
#4245=CARTESIAN_POINT ( 'NONE',  ( 0.2500000000000002220, 0.000000000000000000, 0.000000000000000000 ) ) ;
#4251=LINE ( 'NONE', #995, #6024 ) ;
#4256=LINE ( 'NONE', #22574, #20615 ) ;
#4268=ORIENTED_EDGE ( 'NONE', *, *, #9067, .T. ) ;
#4343=EDGE_CURVE ( 'NONE', #8977, #9649, #975, .T. ) ;
#4353=EDGE_LOOP ( 'NONE', ( #1248, #1184 ) ) ;
#4362=FACE_OUTER_BOUND ( 'NONE', #7081, .T. ) ;
#4371=ADVANCED_FACE ( 'NONE', ( #12269 ), #4458, .T. ) ;
#4390=VECTOR ( 'NONE', #3745, 1000.000000000000000 ) ;
#4395=LINE ( 'NONE', #18778, #11864 ) ;
#4458=CYLINDRICAL_SURFACE ( 'NONE', #2059, 4.250000000000000000 ) ;
#4480=STYLED_ITEM ( 'NONE', ( #18280 ), #6242 ) ;
#4707=PRESENTATION_STYLE_ASSIGNMENT (( #19303 ) ) ;
#4714=LINE ( 'NONE', #6869, #20578 ) ;
#4757=DIRECTION ( 'NONE',  ( 0.000000000000000000, 0.000000000000000000, 1.000000000000000000 ) ) ;
#4773=CARTESIAN_POINT ( 'NONE',  ( 0.000000000000000000, 5.051668046482832750E-16, -4.000000000000000000 ) ) ;
#4826=CARTESIAN_POINT ( 'NONE',  ( 2.500000000000000000, 2.357898499370431722, -2.818925648462311528E-15 ) ) ;
#4831=CARTESIAN_POINT ( 'NONE',  ( 21.00000000000000000, 2.055000000000000160, 0.000000000000000000 ) ) ;
#4867=DIRECTION ( 'NONE',  ( 0.000000000000000000, -1.287488025362403787E-15, -1.000000000000000000 ) ) ;
#4889=EDGE_CURVE ( 'NONE', #22418, #8553, #17142, .T. ) ;
#4913=ORIENTED_EDGE ( 'NONE', *, *, #8339, .T. ) ;
#4963=PLANE ( 'NONE',  #3698 ) ;
#4964=AXIS2_PLACEMENT_3D ( 'NONE', #21250, #4867, #12202 ) ;
#4965=EDGE_CURVE ( 'NONE', #611, #13486, #948, .T. ) ;
#4985=AXIS2_PLACEMENT_3D ( 'NONE', #6617, #15390, #13471 ) ;
#4986=UNCERTAINTY_MEASURE_WITH_UNIT (LENGTH_MEASURE( 1.000000000000000082E-05 ), #15162, 'distance_accuracy_value', 'NONE');
#5046=DIRECTION ( 'NONE',  ( 0.000000000000000000, 0.000000000000000000, 1.000000000000000000 ) ) ;
#5064=DIRECTION ( 'NONE',  ( 0.000000000000000000, -0.4999999999999993339, 0.8660254037844390407 ) ) ;
#5075=CARTESIAN_POINT ( 'NONE',  ( 2.500000000000000000, 2.357898499370431722, -2.818925648462311528E-15 ) ) ;
#5143=CARTESIAN_POINT ( 'NONE',  ( 2.500000000000000000, 0.000000000000000000, 0.000000000000000000 ) ) ;
#5158=EDGE_CURVE ( 'NONE', #22418, #17065, #5186, .T. ) ;
#5161=AXIS2_PLACEMENT_3D ( 'NONE', #15717, #8627, #6950 ) ;
#5172=ORIENTED_EDGE ( 'NONE', *, *, #11592, .F. ) ;
#5186=CIRCLE ( 'NONE', #8270, 2.041999999999999815 ) ;
#5211=ORIENTED_EDGE ( 'NONE', *, *, #13057, .F. ) ;
#5228=CARTESIAN_POINT ( 'NONE',  ( -31.74999999999995737, 0.000000000000000000, 2.500000000000000444 ) ) ;
#5290=AXIS2_PLACEMENT_3D ( 'NONE', #7616, #21845, #9300 ) ;
#5302=EDGE_CURVE ( 'NONE', #7612, #7146, #3549, .T. ) ;
#5338=EDGE_LOOP ( 'NONE', ( #11683, #5436, #21600, #13629, #12518 ) ) ;
#5364=CONICAL_SURFACE ( 'NONE', #777, 2.041999999999999815, 1.047197551196591858 ) ;
#5366=EDGE_CURVE ( 'NONE', #22997, #13902, #4040, .T. ) ;
#5375=EDGE_CURVE ( 'NONE', #18055, #15893, #13255, .T. ) ;
#5384=DIRECTION ( 'NONE',  ( 0.000000000000000000, 0.000000000000000000, 1.000000000000000000 ) ) ;
#5396=AXIS2_PLACEMENT_3D ( 'NONE', #15241, #17138, #2508 ) ;
#5403=DIRECTION ( 'NONE',  ( -1.000000000000000000, -0.000000000000000000, -0.000000000000000000 ) ) ;
#5435=PLANE ( 'NONE',  #20637 ) ;
#5436=ORIENTED_EDGE ( 'NONE', *, *, #23158, .T. ) ;
#5444=CARTESIAN_POINT ( 'NONE',  ( -31.74999999999995737, 0.000000000000000000, 0.000000000000000000 ) ) ;
#5587=ORIENTED_EDGE ( 'NONE', *, *, #5158, .F. ) ;
#5657=EDGE_CURVE ( 'NONE', #23445, #22997, #16395, .T. ) ;
#5664=( GEOMETRIC_REPRESENTATION_CONTEXT ( 3 ) GLOBAL_UNCERTAINTY_ASSIGNED_CONTEXT ( ( #4986 ) ) GLOBAL_UNIT_ASSIGNED_CONTEXT ( ( #15162, #20630, #2190 ) ) REPRESENTATION_CONTEXT ( 'NONE', 'WORKASPACE' ) );
#5716=EDGE_CURVE ( 'NONE', #611, #12043, #7434, .T. ) ;
#5719=CARTESIAN_POINT ( 'NONE',  ( 4.999999999999997335, 0.000000000000000000, 0.000000000000000000 ) ) ;
#5720=AXIS2_PLACEMENT_3D ( 'NONE', #19676, #12536, #3400 ) ;
#5827=ADVANCED_FACE ( 'NONE', ( #20447 ), #11386, .T. ) ;
#5880=DIRECTION ( 'NONE',  ( 0.000000000000000000, -0.5000000000000009992, -0.8660254037844380415 ) ) ;
#5907=FACE_OUTER_BOUND ( 'NONE', #7523, .T. ) ;
#5935=AXIS2_PLACEMENT_3D ( 'NONE', #182, #8849, #21615 ) ;
#5950=EDGE_LOOP ( 'NONE', ( #21380, #20887, #1812, #23096, #18205 ) ) ;
#5966=CARTESIAN_POINT ( 'NONE',  ( 5.000000000000000888, 4.250000000000000000, 0.000000000000000000 ) ) ;
#5976=LINE ( 'NONE', #9952, #6259 ) ;
#5984=EDGE_CURVE ( 'NONE', #8553, #9649, #15579, .T. ) ;
#6024=VECTOR ( 'NONE', #11816, 1000.000000000000000 ) ;
#6060=CARTESIAN_POINT ( 'NONE',  ( 2.500000000000000000, 0.000000000000000000, 0.000000000000000000 ) ) ;
#6102=AXIS2_PLACEMENT_3D ( 'NONE', #21085, #3006, #19647 ) ;
#6130=PRODUCT_CONTEXT ( 'NONE', #7335, 'mechanical' ) ;
#6146=ADVANCED_FACE ( 'NONE', ( #16032 ), #12701, .F. ) ;
#6168=CARTESIAN_POINT ( 'NONE',  ( 2.500000000000000000, 1.178949249685212974, -2.042000000000001148 ) ) ;
#6214=DIRECTION ( 'NONE',  ( 0.000000000000000000, 0.000000000000000000, -1.000000000000000000 ) ) ;
#6217=AXIS2_PLACEMENT_3D ( 'NONE', #11627, #7896, #8019 ) ;
#6242=MANIFOLD_SOLID_BREP ( 'Hex', #11643 ) ;
#6259=VECTOR ( 'NONE', #20213, 1000.000000000000000 ) ;
#6282=FACE_OUTER_BOUND ( 'NONE', #16351, .T. ) ;
#6296=EDGE_CURVE ( 'NONE', #611, #22180, #16728, .T. ) ;
#6314=VERTEX_POINT ( 'NONE', #15077 ) ;
#6322=FACE_OUTER_BOUND ( 'NONE', #12369, .T. ) ;
#6382=LINE ( 'NONE', #20849, #22683 ) ;
#6387=ORIENTED_EDGE ( 'NONE', *, *, #10242, .T. ) ;
#6425=ORIENTED_EDGE ( 'NONE', *, *, #16537, .T. ) ;
#6455=DIRECTION ( 'NONE',  ( -1.000000000000000000, -0.000000000000000000, -0.000000000000000000 ) ) ;
#6480=ORIENTED_EDGE ( 'NONE', *, *, #9820, .T. ) ;
#6498=AXIS2_PLACEMENT_3D ( 'NONE', #20677, #2471, #22347 ) ;
#6510=CARTESIAN_POINT ( 'NONE',  ( 0.000000000000000000, 1.178949249685212974, -2.042000000000001148 ) ) ;
#6516=CARTESIAN_POINT ( 'NONE',  ( 2.500000000000000000, -2.629050547790028551E-15, -2.041999999999999815 ) ) ;
#6617=CARTESIAN_POINT ( 'NONE',  ( 5.000000000000000888, 0.000000000000000000, 0.000000000000000000 ) ) ;
#6675=FACE_OUTER_BOUND ( 'NONE', #12399, .T. ) ;
#6686=CARTESIAN_POINT ( 'NONE',  ( 3.678949249685231848, 0.000000000000000000, 0.000000000000000000 ) ) ;
#6707=SHAPE_REPRESENTATION ( 'socket head cap screw_iso_ISO 4762 M5 x 16 - 16N', ( #7318 ), #5664 ) ;
#6747=SHAPE_REPRESENTATION_RELATIONSHIP ( 'NONE' , 'NONE' ,  #6707, #1883 ) ;
#6820=CARTESIAN_POINT ( 'NONE',  ( 21.00000000000000355, 0.000000000000000000, 0.000000000000000000 ) ) ;
#6832=EDGE_LOOP ( 'NONE', ( #8883, #19025, #13151 ) ) ;
#6869=CARTESIAN_POINT ( 'NONE',  ( 0.000000000000000000, 2.357898499370431722, -2.818925648462311528E-15 ) ) ;
#6875=VECTOR ( 'NONE', #10624, 1000.000000000000114 ) ;
#6889=CIRCLE ( 'NONE', #18748, 2.500000000000000888 ) ;
#6904=ADVANCED_FACE ( 'NONE', ( #6282 ), #3375, .T. ) ;
#6927=AXIS2_PLACEMENT_3D ( 'NONE', #21646, #1291, #10328 ) ;
#6950=DIRECTION ( 'NONE',  ( 0.000000000000000000, 0.000000000000000000, -1.000000000000000000 ) ) ;
#6969=EDGE_CURVE ( 'NONE', #14005, #16753, #3019, .T. ) ;
#7074=DIRECTION ( 'NONE',  ( 0.000000000000000000, 0.000000000000000000, 1.000000000000000000 ) ) ;
#7081=EDGE_LOOP ( 'NONE', ( #8391, #1153, #1458, #12612 ) ) ;
#7113=DIRECTION ( 'NONE',  ( -1.000000000000000000, -0.000000000000000000, -0.000000000000000000 ) ) ;
#7146=VERTEX_POINT ( 'NONE', #2254 ) ;
#7165=DIRECTION ( 'NONE',  ( 0.000000000000000000, 0.000000000000000000, -1.000000000000000000 ) ) ;
#7253=EDGE_LOOP ( 'NONE', ( #22162, #6387 ) ) ;
#7285=ORIENTED_EDGE ( 'NONE', *, *, #11592, .T. ) ;
#7315=AXIS2_PLACEMENT_3D ( 'NONE', #7685, #15003, #13193 ) ;
#7318=AXIS2_PLACEMENT_3D ( 'NONE', #3111, #10686, #17843 ) ;
#7335=APPLICATION_CONTEXT ( 'automotive_design' ) ;
#7374=ADVANCED_FACE ( 'NONE', ( #15346 ), #22485, .T. ) ;
#7376=DIRECTION ( 'NONE',  ( 0.000000000000000000, 0.000000000000000000, -1.000000000000000000 ) ) ;
#7377=LINE ( 'NONE', #11450, #4390 ) ;
#7434=LINE ( 'NONE', #14747, #14058 ) ;
#7464=ORIENTED_EDGE ( 'NONE', *, *, #4965, .T. ) ;
#7520=VERTEX_POINT ( 'NONE', #6686 ) ;
#7523=EDGE_LOOP ( 'NONE', ( #14303, #12118, #12803, #15708 ) ) ;
#7562=VECTOR ( 'NONE', #20416, 999.9999999999997726 ) ;
#7612=VERTEX_POINT ( 'NONE', #8236 ) ;
#7616=CARTESIAN_POINT ( 'NONE',  ( 2.500000000000000000, 0.000000000000000000, 0.000000000000000000 ) ) ;
#7644=ORIENTED_EDGE ( 'NONE', *, *, #6969, .T. ) ;
#7685=CARTESIAN_POINT ( 'NONE',  ( 4.999999999999997335, 0.000000000000000000, 0.000000000000000000 ) ) ;
#7690=CIRCLE ( 'NONE', #7315, 4.250000000000000000 ) ;
#7753=ORIENTED_EDGE ( 'NONE', *, *, #9366, .F. ) ;
#7763=EDGE_LOOP ( 'NONE', ( #13689, #6480, #20356, #7285 ) ) ;
#7787=DIRECTION ( 'NONE',  ( 0.000000000000000000, 0.000000000000000000, 1.000000000000000000 ) ) ;
#7870=( NAMED_UNIT ( * ) SI_UNIT ( $, .STERADIAN. ) SOLID_ANGLE_UNIT ( ) );
#7884=DIRECTION ( 'NONE',  ( -0.7071067811865364705, 0.000000000000000000, 0.7071067811865584529 ) ) ;
#7896=DIRECTION ( 'NONE',  ( -0.000000000000000000, 1.000000000000000000, 1.224646799147353207E-16 ) ) ;
#7899=DIRECTION ( 'NONE',  ( -1.000000000000000000, -0.000000000000000000, -0.000000000000000000 ) ) ;
#7930=TOROIDAL_SURFACE ( 'NONE', #23594, 2.700000000000000622, 0.2000000000000000111 ) ;
#7938=EDGE_CURVE ( 'NONE', #13486, #22180, #2220, .T. ) ;
#7975=VECTOR ( 'NONE', #18736, 1000.000000000000000 ) ;
#7977=COLOUR_RGB ( '', 0.09019608, 0.27058824, 0.51372549) ;
#8019=DIRECTION ( 'NONE',  ( 0.000000000000000000, -1.224646799147353454E-16, 1.000000000000000000 ) ) ;
#8038=ADVANCED_FACE ( 'NONE', ( #3882 ), #11216, .F. ) ;
#8074=VECTOR ( 'NONE', #16912, 1000.000000000000000 ) ;
#8114=CARTESIAN_POINT ( 'NONE',  ( 21.00000000000000355, 2.516649172247811061E-16, -2.055000000000000160 ) ) ;
#8171=EDGE_CURVE ( 'NONE', #19202, #8553, #9657, .T. ) ;
#8175=ORIENTED_EDGE ( 'NONE', *, *, #1966, .T. ) ;
#8228=DIRECTION ( 'NONE',  ( 0.000000000000000000, 0.000000000000000000, 1.000000000000000000 ) ) ;
#8236=CARTESIAN_POINT ( 'NONE',  ( 20.55500000000001748, 0.000000000000000000, 2.500000000000000888 ) ) ;
#8245=EDGE_LOOP ( 'NONE', ( #18912, #1902, #18824, #17481 ) ) ;
#8254=DIRECTION ( 'NONE',  ( -1.000000000000000000, -0.000000000000000000, -0.000000000000000000 ) ) ;
#8263=ORIENTED_EDGE ( 'NONE', *, *, #12761, .F. ) ;
#8270=AXIS2_PLACEMENT_3D ( 'NONE', #13647, #8254, #4757 ) ;
#8325=ADVANCED_FACE ( 'NONE', ( #23029 ), #21451, .F. ) ;
#8339=EDGE_CURVE ( 'NONE', #12043, #428, #4714, .T. ) ;
#8354=AXIS2_PLACEMENT_3D ( 'NONE', #18492, #1608, #2075 ) ;
#8355=PRODUCT_DEFINITION_CONTEXT ( 'detailed design', #2570, 'design' ) ;
#8391=ORIENTED_EDGE ( 'NONE', *, *, #5375, .T. ) ;
#8400=EDGE_CURVE ( 'NONE', #7146, #13567, #19379, .T. ) ;
#8435=DIRECTION ( 'NONE',  ( 0.000000000000000000, 0.000000000000000000, 1.000000000000000000 ) ) ;
#8444=SURFACE_STYLE_FILL_AREA ( #17177 ) ;
#8461=AXIS2_PLACEMENT_3D ( 'NONE', #6060, #17083, #8228 ) ;
#8464=CIRCLE ( 'NONE', #8842, 2.041999999999999815 ) ;
#8510=EDGE_CURVE ( 'NONE', #13902, #22997, #2167, .T. ) ;
#8553=VERTEX_POINT ( 'NONE', #23418 ) ;
#8557=ORIENTED_EDGE ( 'NONE', *, *, #2051, .F. ) ;
#8627=DIRECTION ( 'NONE',  ( 1.000000000000000000, 0.000000000000000000, 0.000000000000000000 ) ) ;
#8628=CONICAL_SURFACE ( 'NONE', #9777, 2.041999999999999815, 1.047197551196591858 ) ;
#8773=AXIS2_PLACEMENT_3D ( 'NONE', #1586, #10380, #3272 ) ;
#8794=ORIENTED_EDGE ( 'NONE', *, *, #10412, .T. ) ;
#8827=FACE_OUTER_BOUND ( 'NONE', #16463, .T. ) ;
#8842=AXIS2_PLACEMENT_3D ( 'NONE', #20830, #15482, #22753 ) ;
#8849=DIRECTION ( 'NONE',  ( 0.000000000000000000, 0.8660254037844380415, -0.5000000000000009992 ) ) ;
#8851=ORIENTED_EDGE ( 'NONE', *, *, #23627, .T. ) ;
#8883=ORIENTED_EDGE ( 'NONE', *, *, #8171, .T. ) ;
#8892=CARTESIAN_POINT ( 'NONE',  ( 2.500000000000000000, -1.178949249685214307, 2.042000000000001592 ) ) ;
#8893=DIRECTION ( 'NONE',  ( 0.000000000000000000, 1.000000000000000000, -1.287488025362403787E-15 ) ) ;
#8977=VERTEX_POINT ( 'NONE', #15844 ) ;
#8989=CARTESIAN_POINT ( 'NONE',  ( 2.500000000000000000, 2.629050547790028946E-15, 2.042000000000000259 ) ) ;
#9015=LINE ( 'NONE', #17978, #3786 ) ;
#9067=EDGE_CURVE ( 'NONE', #9624, #428, #9015, .T. ) ;
#9087=ORIENTED_EDGE ( 'NONE', *, *, #23158, .F. ) ;
#9113=DIRECTION ( 'NONE',  ( -1.000000000000000000, -0.000000000000000000, -0.000000000000000000 ) ) ;
#9122=DIRECTION ( 'NONE',  ( 0.000000000000000000, -1.000000000000000000, 0.000000000000000000 ) ) ;
#9160=DIRECTION ( 'NONE',  ( 0.000000000000000000, 0.000000000000000000, -1.000000000000000000 ) ) ;
#9180=LINE ( 'NONE', #12774, #1314 ) ;
#9300=DIRECTION ( 'NONE',  ( 0.000000000000000000, 0.000000000000000000, 1.000000000000000000 ) ) ;
#9366=EDGE_CURVE ( 'NONE', #7146, #3630, #15319, .T. ) ;
#9416=AXIS2_PLACEMENT_3D ( 'NONE', #19831, #18052, #10657 ) ;
#9489=CIRCLE ( 'NONE', #12955, 4.250000000000000000 ) ;
#9560=ORIENTED_EDGE ( 'NONE', *, *, #10242, .F. ) ;
#9601=ORIENTED_EDGE ( 'NONE', *, *, #19152, .T. ) ;
#9624=VERTEX_POINT ( 'NONE', #23688 ) ;
#9639=CARTESIAN_POINT ( 'NONE',  ( 2.500000000000000000, -1.178949249685214307, 2.042000000000001592 ) ) ;
#9641=DIRECTION ( 'NONE',  ( 0.000000000000000000, 0.000000000000000000, 1.000000000000000000 ) ) ;
#9647=ORIENTED_EDGE ( 'NONE', *, *, #5984, .T. ) ;
#9649=VERTEX_POINT ( 'NONE', #18293 ) ;
#9657=LINE ( 'NONE', #6168, #7975 ) ;
#9777=AXIS2_PLACEMENT_3D ( 'NONE', #5143, #23467, #7074 ) ;
#9820=EDGE_CURVE ( 'NONE', #14005, #19193, #1847, .T. ) ;
#9883=ORIENTED_EDGE ( 'NONE', *, *, #17251, .F. ) ;
#9946=DIRECTION ( 'NONE',  ( 0.000000000000000000, -1.000000000000000000, 0.000000000000000000 ) ) ;
#9952=CARTESIAN_POINT ( 'NONE',  ( -31.74999999999995737, 0.000000000000000000, 4.250000000000000000 ) ) ;
#9959=DIRECTION ( 'NONE',  ( 1.000000000000000000, 0.000000000000000000, 0.000000000000000000 ) ) ;
#9963=EDGE_CURVE ( 'NONE', #13999, #2500, #14673, .T. ) ;
#10047=VERTEX_POINT ( 'NONE', #16456 ) ;
#10087=ORIENTED_EDGE ( 'NONE', *, *, #7938, .F. ) ;
#10106=AXIS2_PLACEMENT_3D ( 'NONE', #12943, #18194, #5384 ) ;
#10157=AXIS2_PLACEMENT_3D ( 'NONE', #6820, #1182, #10326 ) ;
#10169=CIRCLE ( 'NONE', #10931, 0.2000000000000000944 ) ;
#10229=DIRECTION ( 'NONE',  ( 0.000000000000000000, -0.5000000000000013323, -0.8660254037844380415 ) ) ;
#10233=CARTESIAN_POINT ( 'NONE',  ( 2.500000000000000000, 1.768423874527822459, -1.021000000000002794 ) ) ;
#10242=EDGE_CURVE ( 'NONE', #3630, #15866, #15333, .T. ) ;
#10246=DIRECTION ( 'NONE',  ( -1.000000000000000000, -0.000000000000000000, -0.000000000000000000 ) ) ;
#10252=CARTESIAN_POINT ( 'NONE',  ( 2.500000000000000000, 1.768423874527823791, 1.020999999999998353 ) ) ;
#10276=ORIENTED_EDGE ( 'NONE', *, *, #23598, .F. ) ;
#10302=STYLED_ITEM ( 'NONE', ( #4707 ), #1883 ) ;
#10326=DIRECTION ( 'NONE',  ( 0.000000000000000000, 0.000000000000000000, 1.000000000000000000 ) ) ;
#10328=DIRECTION ( 'NONE',  ( 0.000000000000000000, 0.000000000000000000, 1.000000000000000000 ) ) ;
#10336=EDGE_LOOP ( 'NONE', ( #2459, #7644, #13590, #10610 ) ) ;
#10357=CARTESIAN_POINT ( 'NONE',  ( -31.74999999999995737, 0.000000000000000000, 0.000000000000000000 ) ) ;
#10380=DIRECTION ( 'NONE',  ( -1.000000000000000000, -0.000000000000000000, -0.000000000000000000 ) ) ;
#10407=ADVANCED_FACE ( 'NONE', ( #14171 ), #1317, .T. ) ;
#10412=EDGE_CURVE ( 'NONE', #17390, #17065, #3002, .T. ) ;
#10423=CARTESIAN_POINT ( 'NONE',  ( 21.00000000000000355, 0.000000000000000000, 0.000000000000000000 ) ) ;
#10441=EDGE_CURVE ( 'NONE', #13567, #7146, #21367, .T. ) ;
#10610=ORIENTED_EDGE ( 'NONE', *, *, #3635, .F. ) ;
#10624=DIRECTION ( 'NONE',  ( 0.000000000000000000, 0.4999999999999990008, -0.8660254037844391517 ) ) ;
#10651=FACE_OUTER_BOUND ( 'NONE', #21711, .T. ) ;
#10657=DIRECTION ( 'NONE',  ( 0.000000000000000000, 0.000000000000000000, 1.000000000000000000 ) ) ;
#10686=DIRECTION ( 'NONE',  ( 0.000000000000000000, 0.000000000000000000, 1.000000000000000000 ) ) ;
#10700=AXIS2_PLACEMENT_3D ( 'NONE', #21306, #5403, #5046 ) ;
#10715=VERTEX_POINT ( 'NONE', #18806 ) ;
#10727=ORIENTED_EDGE ( 'NONE', *, *, #16537, .F. ) ;
#10778=DIRECTION ( 'NONE',  ( 0.000000000000000000, 0.000000000000000000, 1.000000000000000000 ) ) ;
#10803=PRODUCT_DEFINITION ( 'UNKNOWN', '', #20984, #8355 ) ;
#10806=DIRECTION ( 'NONE',  ( -1.000000000000000000, -0.000000000000000000, -0.000000000000000000 ) ) ;
#10817=DIRECTION ( 'NONE',  ( 0.000000000000000000, 1.000000000000000000, -1.287488025362403787E-15 ) ) ;
#10824=DIRECTION ( 'NONE',  ( 0.000000000000000000, 0.000000000000000000, 1.000000000000000000 ) ) ;
#10931=AXIS2_PLACEMENT_3D ( 'NONE', #22611, #9946, #6214 ) ;
#10965=CARTESIAN_POINT ( 'NONE',  ( 2.500000000000000000, -2.357898499370432166, 3.035766082959412415E-15 ) ) ;
#10969=ORIENTED_EDGE ( 'NONE', *, *, #13812, .F. ) ;
#11133=VECTOR ( 'NONE', #1684, 1000.000000000000114 ) ;
#11216=PLANE ( 'NONE',  #8354 ) ;
#11256=FACE_OUTER_BOUND ( 'NONE', #16667, .T. ) ;
#11280=VECTOR ( 'NONE', #2887, 1000.000000000000000 ) ;
#11352=EDGE_CURVE ( 'NONE', #9624, #6314, #15014, .T. ) ;
#11360=ORIENTED_EDGE ( 'NONE', *, *, #9067, .F. ) ;
#11375=PLANE ( 'NONE',  #18518 ) ;
#11386=CYLINDRICAL_SURFACE ( 'NONE', #20579, 2.500000000000000444 ) ;
#11404=AXIS2_PLACEMENT_3D ( 'NONE', #19954, #23321, #7165 ) ;
#11444=AXIS2_PLACEMENT_3D ( 'NONE', #1778, #9122, #16411 ) ;
#11450=CARTESIAN_POINT ( 'NONE',  ( 2.500000000000000000, 2.357898499370431722, -2.818925648462311528E-15 ) ) ;
#11467=ADVANCED_FACE ( 'NONE', ( #17021, #20936 ), #19037, .T. ) ;
#11479=ORIENTED_EDGE ( 'NONE', *, *, #5657, .T. ) ;
#11496=UNCERTAINTY_MEASURE_WITH_UNIT (LENGTH_MEASURE( 1.000000000000000082E-05 ), #16970, 'distance_accuracy_value', 'NONE');
#11592=EDGE_CURVE ( 'NONE', #23445, #16753, #804, .T. ) ;
#11627=CARTESIAN_POINT ( 'NONE',  ( 0.2500000000000002220, 4.898587196589412829E-16, -4.000000000000000000 ) ) ;
#11641=CARTESIAN_POINT ( 'NONE',  ( 2.500000000000000000, -1.178949249685214307, 2.042000000000001592 ) ) ;
#11643=CLOSED_SHELL ( 'NONE', ( #23253, #2640, #17284, #15112, #20038, #10407, #11467, #4371, #4126, #5827, #1761, #13454, #1285, #6904, #16220, #12903, #17894, #7374, #16260, #15703, #12497, #8038, #8325, #1610, #22639, #6146, #19610 ) ) ;
#11683=ORIENTED_EDGE ( 'NONE', *, *, #21636, .F. ) ;
#11705=CARTESIAN_POINT ( 'NONE',  ( 0.2500000000000002220, 5.204748896376250699E-16, -4.250000000000000000 ) ) ;
#11816=DIRECTION ( 'NONE',  ( -1.000000000000000000, -0.000000000000000000, -0.000000000000000000 ) ) ;
#11820=LINE ( 'NONE', #15417, #15083 ) ;
#11855=EDGE_CURVE ( 'NONE', #10715, #7612, #6889, .T. ) ;
#11864=VECTOR ( 'NONE', #7884, 1000.000000000000114 ) ;
#12006=CARTESIAN_POINT ( 'NONE',  ( 2.500000000000000000, 2.357898499370431722, -2.818925648462311528E-15 ) ) ;
#12043=VERTEX_POINT ( 'NONE', #808 ) ;
#12077=ORIENTED_EDGE ( 'NONE', *, *, #12789, .F. ) ;
#12079=AXIS2_PLACEMENT_3D ( 'NONE', #5444, #21714, #16125 ) ;
#12103=ORIENTED_EDGE ( 'NONE', *, *, #19183, .T. ) ;
#12118=ORIENTED_EDGE ( 'NONE', *, *, #17251, .T. ) ;
#12157=DIRECTION ( 'NONE',  ( 1.000000000000000000, 0.000000000000000000, 0.000000000000000000 ) ) ;
#12202=DIRECTION ( 'NONE',  ( 0.000000000000000000, 1.000000000000000000, -1.287488025362403787E-15 ) ) ;
#12269=FACE_OUTER_BOUND ( 'NONE', #7763, .T. ) ;
#12297=DIRECTION ( 'NONE',  ( 0.000000000000000000, 0.000000000000000000, -1.000000000000000000 ) ) ;
#12312=ORIENTED_EDGE ( 'NONE', *, *, #13349, .F. ) ;
#12369=EDGE_LOOP ( 'NONE', ( #22299, #1724, #7464, #12103, #2424 ) ) ;
#12397=EDGE_LOOP ( 'NONE', ( #9087, #21623, #2576, #13328, #3298 ) ) ;
#12399=EDGE_LOOP ( 'NONE', ( #18442, #22588, #18510, #2850, #8851 ) ) ;
#12462=EDGE_CURVE ( 'NONE', #22180, #19202, #14947, .T. ) ;
#12497=ADVANCED_FACE ( 'NONE', ( #3050 ), #16121, .F. ) ;
#12518=ORIENTED_EDGE ( 'NONE', *, *, #12462, .T. ) ;
#12536=DIRECTION ( 'NONE',  ( -1.000000000000000000, -0.000000000000000000, -0.000000000000000000 ) ) ;
#12612=ORIENTED_EDGE ( 'NONE', *, *, #15979, .F. ) ;
#12633=FACE_OUTER_BOUND ( 'NONE', #12397, .T. ) ;
#12654=CIRCLE ( 'NONE', #20646, 2.041999999999999815 ) ;
#12682=VECTOR ( 'NONE', #10817, 1000.000000000000000 ) ;
#12701=PLANE ( 'NONE',  #11404 ) ;
#12761=EDGE_CURVE ( 'NONE', #17390, #13999, #14401, .T. ) ;
#12770=CARTESIAN_POINT ( 'NONE',  ( 2.500000000000000000, 2.357898499370431722, -2.818925648462311528E-15 ) ) ;
#12774=CARTESIAN_POINT ( 'NONE',  ( 2.500000000000000000, 2.357898499370431722, -2.818925648462311528E-15 ) ) ;
#12789=EDGE_CURVE ( 'NONE', #17390, #9624, #23475, .T. ) ;
#12803=ORIENTED_EDGE ( 'NONE', *, *, #15979, .T. ) ;
#12804=ORIENTED_EDGE ( 'NONE', *, *, #5375, .F. ) ;
#12903=ADVANCED_FACE ( 'NONE', ( #22372 ), #17009, .F. ) ;
#12914=ORIENTED_EDGE ( 'NONE', *, *, #2896, .T. ) ;
#12936=MECHANICAL_DESIGN_GEOMETRIC_PRESENTATION_REPRESENTATION('',(#4480),#2183);
#12943=CARTESIAN_POINT ( 'NONE',  ( 0.2500000000000002220, 0.000000000000000000, 0.000000000000000000 ) ) ;
#12955=AXIS2_PLACEMENT_3D ( 'NONE', #13790, #9959, #21046 ) ;
#12963=DIRECTION ( 'NONE',  ( 1.000000000000000000, 0.000000000000000000, 0.000000000000000000 ) ) ;
#12970=DIRECTION ( 'NONE',  ( -1.000000000000000000, -0.000000000000000000, -0.000000000000000000 ) ) ;
#13020=EDGE_CURVE ( 'NONE', #10715, #13567, #15226, .T. ) ;
#13057=EDGE_CURVE ( 'NONE', #19193, #14005, #7690, .T. ) ;
#13151=ORIENTED_EDGE ( 'NONE', *, *, #16881, .F. ) ;
#13159=UNCERTAINTY_MEASURE_WITH_UNIT (LENGTH_MEASURE( 1.000000000000000082E-05 ), #21322, 'distance_accuracy_value', 'NONE');
#13174=CARTESIAN_POINT ( 'NONE',  ( 20.55500000000001748, 0.000000000000000000, 0.000000000000000000 ) ) ;
#13193=DIRECTION ( 'NONE',  ( 0.000000000000000000, 0.000000000000000000, 1.000000000000000000 ) ) ;
#13255=CIRCLE ( 'NONE', #15173, 2.055000000000000160 ) ;
#13281=DIRECTION ( 'NONE',  ( -1.000000000000000000, -0.000000000000000000, -0.000000000000000000 ) ) ;
#13301=CARTESIAN_POINT ( 'NONE',  ( 2.500000000000000000, -2.357898499370432166, 3.035766082959412415E-15 ) ) ;
#13307=DIRECTION ( 'NONE',  ( 0.000000000000000000, -1.000000000000000000, 1.287488025362403787E-15 ) ) ;
#13328=ORIENTED_EDGE ( 'NONE', *, *, #5158, .T. ) ;
#13349=EDGE_CURVE ( 'NONE', #10047, #6314, #4251, .T. ) ;
#13352=AXIS2_PLACEMENT_3D ( 'NONE', #4826, #12157, #17537 ) ;
#13396=ORIENTED_EDGE ( 'NONE', *, *, #2896, .F. ) ;
#13414=AXIS2_PLACEMENT_3D ( 'NONE', #5719, #13281, #3910 ) ;
#13454=ADVANCED_FACE ( 'NONE', ( #529 ), #2794, .T. ) ;
#13471=DIRECTION ( 'NONE',  ( 0.000000000000000000, 0.000000000000000000, -1.000000000000000000 ) ) ;
#13486=VERTEX_POINT ( 'NONE', #10252 ) ;
#13547=DIRECTION ( 'NONE',  ( 0.000000000000000000, 1.000000000000000000, -1.224646799147353207E-16 ) ) ;
#13567=VERTEX_POINT ( 'NONE', #23266 ) ;
#13590=ORIENTED_EDGE ( 'NONE', *, *, #13812, .T. ) ;
#13617=LINE ( 'NONE', #8114, #765 ) ;
#13629=ORIENTED_EDGE ( 'NONE', *, *, #7938, .T. ) ;
#13647=CARTESIAN_POINT ( 'NONE',  ( 2.500000000000000000, 0.000000000000000000, 0.000000000000000000 ) ) ;
#13654=DIRECTION ( 'NONE',  ( 0.000000000000000000, -0.4999999999999989453, 0.8660254037844391517 ) ) ;
#13689=ORIENTED_EDGE ( 'NONE', *, *, #6969, .F. ) ;
#13726=( GEOMETRIC_REPRESENTATION_CONTEXT ( 3 ) GLOBAL_UNCERTAINTY_ASSIGNED_CONTEXT ( ( #13159 ) ) GLOBAL_UNIT_ASSIGNED_CONTEXT ( ( #21322, #2781, #759 ) ) REPRESENTATION_CONTEXT ( 'NONE', 'WORKASPACE' ) );
#13761=CIRCLE ( 'NONE', #6102, 2.041999999999999815 ) ;
#13790=CARTESIAN_POINT ( 'NONE',  ( 0.2500000000000002220, 0.000000000000000000, 0.000000000000000000 ) ) ;
#13793=VECTOR ( 'NONE', #2303, 1000.000000000000000 ) ;
#13812=EDGE_CURVE ( 'NONE', #16753, #23445, #9489, .T. ) ;
#13902=VERTEX_POINT ( 'NONE', #4773 ) ;
#13947=ORIENTED_EDGE ( 'NONE', *, *, #19977, .T. ) ;
#13955=VERTEX_POINT ( 'NONE', #19727 ) ;
#13988=PLANE ( 'NONE',  #4964 ) ;
#13999=VERTEX_POINT ( 'NONE', #8989 ) ;
#14005=VERTEX_POINT ( 'NONE', #19608 ) ;
#14024=CARTESIAN_POINT ( 'NONE',  ( 2.500000000000000000, 1.178949249685217415, 2.041999999999998483 ) ) ;
#14029=EDGE_LOOP ( 'NONE', ( #1456, #14356, #3937, #2188 ) ) ;
#14058=VECTOR ( 'NONE', #7899, 1000.000000000000000 ) ;
#14171=FACE_OUTER_BOUND ( 'NONE', #10336, .T. ) ;
#14189=VECTOR ( 'NONE', #19986, 1000.000000000000000 ) ;
#14303=ORIENTED_EDGE ( 'NONE', *, *, #22526, .F. ) ;
#14356=ORIENTED_EDGE ( 'NONE', *, *, #9366, .T. ) ;
#14401=LINE ( 'NONE', #8892, #12682 ) ;
#14476=DIRECTION ( 'NONE',  ( -1.000000000000000000, -0.000000000000000000, -0.000000000000000000 ) ) ;
#14532=DIRECTION ( 'NONE',  ( 0.000000000000000000, -0.5000000000000009992, -0.8660254037844380415 ) ) ;
#14666=CARTESIAN_POINT ( 'NONE',  ( 0.000000000000000000, 0.000000000000000000, 0.000000000000000000 ) ) ;
#14673=LINE ( 'NONE', #9639, #13793 ) ;
#14747=CARTESIAN_POINT ( 'NONE',  ( 2.500000000000000000, 2.357898499370431722, -2.818925648462311528E-15 ) ) ;
#14835=SURFACE_SIDE_STYLE ('',( #434 ) ) ;
#14880=MECHANICAL_DESIGN_GEOMETRIC_PRESENTATION_REPRESENTATION('',(#10302),#13726);
#14901=VECTOR ( 'NONE', #21979, 1000.000000000000114 ) ;
#14947=CIRCLE ( 'NONE', #8461, 2.041999999999999815 ) ;
#15003=DIRECTION ( 'NONE',  ( -1.000000000000000000, -0.000000000000000000, -0.000000000000000000 ) ) ;
#15014=LINE ( 'NONE', #22268, #2328 ) ;
#15077=CARTESIAN_POINT ( 'NONE',  ( 0.000000000000000000, -2.357898499370432166, 3.035766082959412415E-15 ) ) ;
#15083=VECTOR ( 'NONE', #22678, 1000.000000000000000 ) ;
#15112=ADVANCED_FACE ( 'NONE', ( #4362 ), #20978, .T. ) ;
#15162=( LENGTH_UNIT ( ) NAMED_UNIT ( * ) SI_UNIT ( .MILLI., .METRE. ) );
#15173=AXIS2_PLACEMENT_3D ( 'NONE', #10423, #3437, #10778 ) ;
#15226=LINE ( 'NONE', #4063, #21032 ) ;
#15241=CARTESIAN_POINT ( 'NONE',  ( 0.000000000000000000, 0.000000000000000000, 0.000000000000000000 ) ) ;
#15319=CIRCLE ( 'NONE', #20224, 0.2000000000000000944 ) ;
#15321=EDGE_LOOP ( 'NONE', ( #9601, #22901, #20628 ) ) ;
#15333=CIRCLE ( 'NONE', #4985, 2.700000000000000622 ) ;
#15346=FACE_OUTER_BOUND ( 'NONE', #21538, .T. ) ;
#15390=DIRECTION ( 'NONE',  ( -1.000000000000000000, -0.000000000000000000, -0.000000000000000000 ) ) ;
#15417=CARTESIAN_POINT ( 'NONE',  ( 2.500000000000000000, 1.178949249685217415, 2.041999999999998483 ) ) ;
#15482=DIRECTION ( 'NONE',  ( -1.000000000000000000, -0.000000000000000000, -0.000000000000000000 ) ) ;
#15502=CARTESIAN_POINT ( 'NONE',  ( 0.000000000000000000, -2.357898499370432166, 3.035766082959412415E-15 ) ) ;
#15531=CARTESIAN_POINT ( 'NONE',  ( 0.000000000000000000, 1.178949249685217415, 2.041999999999998483 ) ) ;
#15564=DIRECTION ( 'NONE',  ( 0.000000000000000000, 0.4999999999999992784, -0.8660254037844389297 ) ) ;
#15579=LINE ( 'NONE', #22843, #2613 ) ;
#15591=DIRECTION ( 'NONE',  ( 0.000000000000000000, 0.5000000000000011102, 0.8660254037844379305 ) ) ;
#15606=EDGE_LOOP ( 'NONE', ( #4268, #21009, #16921, #8263, #1245 ) ) ;
#15628=CARTESIAN_POINT ( 'NONE',  ( 0.000000000000000000, 0.000000000000000000, 4.000000000000000000 ) ) ;
#15703=ADVANCED_FACE ( 'NONE', ( #17489 ), #17369, .F. ) ;
#15708=ORIENTED_EDGE ( 'NONE', *, *, #11855, .F. ) ;
#15717=CARTESIAN_POINT ( 'NONE',  ( 5.200000000000002842, 0.000000000000000000, 0.000000000000000000 ) ) ;
#15844=CARTESIAN_POINT ( 'NONE',  ( 0.000000000000000000, 1.178949249685212974, -2.042000000000001148 ) ) ;
#15866=VERTEX_POINT ( 'NONE', #21991 ) ;
#15893=VERTEX_POINT ( 'NONE', #2358 ) ;
#15933=ORIENTED_EDGE ( 'NONE', *, *, #11352, .F. ) ;
#15965=ORIENTED_EDGE ( 'NONE', *, *, #1966, .F. ) ;
#15970=ORIENTED_EDGE ( 'NONE', *, *, #13349, .T. ) ;
#15972=AXIS2_PLACEMENT_3D ( 'NONE', #14666, #7113, #18229 ) ;
#15979=EDGE_CURVE ( 'NONE', #18055, #7612, #4395, .T. ) ;
#16032=FACE_OUTER_BOUND ( 'NONE', #15321, .T. ) ;
#16094=EDGE_CURVE ( 'NONE', #15866, #3630, #21369, .T. ) ;
#16116=DIRECTION ( 'NONE',  ( 0.000000000000000000, 0.000000000000000000, -1.000000000000000000 ) ) ;
#16117=ORIENTED_EDGE ( 'NONE', *, *, #5302, .F. ) ;
#16121=PLANE ( 'NONE',  #2313 ) ;
#16125=DIRECTION ( 'NONE',  ( 0.000000000000000000, 0.000000000000000000, 1.000000000000000000 ) ) ;
#16201=CARTESIAN_POINT ( 'NONE',  ( 2.500000000000000000, 0.000000000000000000, 2.041999999999999815 ) ) ;
#16209=ORIENTED_EDGE ( 'NONE', *, *, #11352, .T. ) ;
#16220=ADVANCED_FACE ( 'NONE', ( #6322 ), #1027, .T. ) ;
#16260=ADVANCED_FACE ( 'NONE', ( #6675 ), #13988, .F. ) ;
#16313=DIRECTION ( 'NONE',  ( 1.000000000000000000, 0.000000000000000000, 0.000000000000000000 ) ) ;
#16351=EDGE_LOOP ( 'NONE', ( #13396, #5172, #11479, #695 ) ) ;
#16395=CIRCLE ( 'NONE', #11444, 0.2500000000000002220 ) ;
#16399=DIRECTION ( 'NONE',  ( 1.000000000000000000, 0.000000000000000000, 0.000000000000000000 ) ) ;
#16411=DIRECTION ( 'NONE',  ( 0.000000000000000000, 0.000000000000000000, -1.000000000000000000 ) ) ;
#16456=CARTESIAN_POINT ( 'NONE',  ( 2.500000000000000000, -2.357898499370432166, 3.035766082959412415E-15 ) ) ;
#16463=EDGE_LOOP ( 'NONE', ( #2350, #22758, #19981, #16117 ) ) ;
#16529=ORIENTED_EDGE ( 'NONE', *, *, #9963, .T. ) ;
#16537=EDGE_CURVE ( 'NONE', #17065, #10047, #4256, .T. ) ;
#16577=EDGE_LOOP ( 'NONE', ( #577, #18704, #10276 ) ) ;
#16667=EDGE_LOOP ( 'NONE', ( #5211, #20699 ) ) ;
#16721=ORIENTED_EDGE ( 'NONE', *, *, #19183, .F. ) ;
#16728=LINE ( 'NONE', #22215, #7562 ) ;
#16753=VERTEX_POINT ( 'NONE', #11705 ) ;
#16881=EDGE_CURVE ( 'NONE', #19202, #22418, #12654, .T. ) ;
#16898=CARTESIAN_POINT ( 'NONE',  ( 5.200000000000002842, 3.306546357697854226E-16, 2.700000000000000622 ) ) ;
#16912=DIRECTION ( 'NONE',  ( 0.000000000000000000, -1.000000000000000000, 1.287488025362403787E-15 ) ) ;
#16921=ORIENTED_EDGE ( 'NONE', *, *, #9963, .F. ) ;
#16970=( LENGTH_UNIT ( ) NAMED_UNIT ( * ) SI_UNIT ( .MILLI., .METRE. ) );
#17009=PLANE ( 'NONE',  #3834 ) ;
#17021=FACE_BOUND ( 'NONE', #17849, .T. ) ;
#17065=VERTEX_POINT ( 'NONE', #18687 ) ;
#17083=DIRECTION ( 'NONE',  ( -1.000000000000000000, -0.000000000000000000, -0.000000000000000000 ) ) ;
#17138=DIRECTION ( 'NONE',  ( -1.000000000000000000, 0.000000000000000000, -0.000000000000000000 ) ) ;
#17142=LINE ( 'NONE', #2749, #22393 ) ;
#17177=FILL_AREA_STYLE ('',( #22903 ) ) ;
#17251=EDGE_CURVE ( 'NONE', #15893, #18055, #2085, .T. ) ;
#17284=ADVANCED_FACE ( 'NONE', ( #17374 ), #21592, .F. ) ;
#17300=SURFACE_SIDE_STYLE ('',( #8444 ) ) ;
#17369=PLANE ( 'NONE',  #3402 ) ;
#17374=FACE_OUTER_BOUND ( 'NONE', #14029, .T. ) ;
#17390=VERTEX_POINT ( 'NONE', #17837 ) ;
#17481=ORIENTED_EDGE ( 'NONE', *, *, #8400, .T. ) ;
#17489=FACE_OUTER_BOUND ( 'NONE', #5950, .T. ) ;
#17499=CARTESIAN_POINT ( 'NONE',  ( 2.500000000000000000, 1.178949249685212974, -2.042000000000001148 ) ) ;
#17520=DIRECTION ( 'NONE',  ( 0.000000000000000000, 0.4999999999999990008, -0.8660254037844391517 ) ) ;
#17537=DIRECTION ( 'NONE',  ( 0.000000000000000000, 0.000000000000000000, -1.000000000000000000 ) ) ;
#17579=VECTOR ( 'NONE', #10806, 1000.000000000000000 ) ;
#17643=DIRECTION ( 'NONE',  ( 0.000000000000000000, 0.000000000000000000, -1.000000000000000000 ) ) ;
#17692=CIRCLE ( 'NONE', #6217, 0.2500000000000002220 ) ;
#17733=ORIENTED_EDGE ( 'NONE', *, *, #5366, .F. ) ;
#17832=DIRECTION ( 'NONE',  ( 0.000000000000000000, 0.8660254037844380415, -0.5000000000000012212 ) ) ;
#17837=CARTESIAN_POINT ( 'NONE',  ( 2.500000000000000000, -1.178949249685214307, 2.042000000000001592 ) ) ;
#17843=DIRECTION ( 'NONE',  ( 1.000000000000000000, 0.000000000000000000, 0.000000000000000000 ) ) ;
#17849=EDGE_LOOP ( 'NONE', ( #4913, #11360, #16209, #8175, #21744, #8557 ) ) ;
#17862=CARTESIAN_POINT ( 'NONE',  ( 5.200000000000002842, 0.000000000000000000, 0.000000000000000000 ) ) ;
#17894=ADVANCED_FACE ( 'NONE', ( #10651 ), #18392, .T. ) ;
#17899=DIRECTION ( 'NONE',  ( 1.000000000000000000, 0.000000000000000000, 0.000000000000000000 ) ) ;
#17978=CARTESIAN_POINT ( 'NONE',  ( 0.000000000000000000, -1.178949249685214307, 2.042000000000001592 ) ) ;
#18052=DIRECTION ( 'NONE',  ( -1.000000000000000000, -0.000000000000000000, -0.000000000000000000 ) ) ;
#18055=VERTEX_POINT ( 'NONE', #2211 ) ;
#18086=ORIENTED_EDGE ( 'NONE', *, *, #22120, .F. ) ;
#18194=DIRECTION ( 'NONE',  ( -1.000000000000000000, -0.000000000000000000, -0.000000000000000000 ) ) ;
#18205=ORIENTED_EDGE ( 'NONE', *, *, #5716, .T. ) ;
#18229=DIRECTION ( 'NONE',  ( 0.000000000000000000, 0.000000000000000000, 1.000000000000000000 ) ) ;
#18280=PRESENTATION_STYLE_ASSIGNMENT (( #20300 ) ) ;
#18293=CARTESIAN_POINT ( 'NONE',  ( 0.000000000000000000, -1.178949249685218748, -2.041999999999998039 ) ) ;
#18343=LINE ( 'NONE', #1923, #8074 ) ;
#18363=DIRECTION ( 'NONE',  ( -1.000000000000000000, -0.000000000000000000, -0.000000000000000000 ) ) ;
#18392=PLANE ( 'NONE',  #5935 ) ;
#18442=ORIENTED_EDGE ( 'NONE', *, *, #4343, .T. ) ;
#18492=CARTESIAN_POINT ( 'NONE',  ( 2.500000000000000000, 2.357898499370431722, -2.818925648462311528E-15 ) ) ;
#18510=ORIENTED_EDGE ( 'NONE', *, *, #8171, .F. ) ;
#18515=LINE ( 'NONE', #3556, #14901 ) ;
#18518=AXIS2_PLACEMENT_3D ( 'NONE', #5966, #16399, #92 ) ;
#18636=( NAMED_UNIT ( * ) PLANE_ANGLE_UNIT ( ) SI_UNIT ( $, .RADIAN. ) );
#18687=CARTESIAN_POINT ( 'NONE',  ( 2.500000000000000000, -1.768423874527823569, 1.021000000000002350 ) ) ;
#18704=ORIENTED_EDGE ( 'NONE', *, *, #12761, .T. ) ;
#18736=DIRECTION ( 'NONE',  ( 0.000000000000000000, -1.000000000000000000, 1.287488025362403787E-15 ) ) ;
#18748=AXIS2_PLACEMENT_3D ( 'NONE', #13174, #9113, #20439 ) ;
#18778=CARTESIAN_POINT ( 'NONE',  ( 21.00000000000000355, 0.000000000000000000, 2.055000000000000160 ) ) ;
#18806=CARTESIAN_POINT ( 'NONE',  ( 20.55500000000001748, 3.061616997868384127E-16, -2.500000000000000888 ) ) ;
#18824=ORIENTED_EDGE ( 'NONE', *, *, #5302, .T. ) ;
#18912=ORIENTED_EDGE ( 'NONE', *, *, #13020, .F. ) ;
#19024=AXIS2_PLACEMENT_3D ( 'NONE', #4831, #12963, #1343 ) ;
#19025=ORIENTED_EDGE ( 'NONE', *, *, #4889, .F. ) ;
#19037=PLANE ( 'NONE',  #5396 ) ;
#19152=EDGE_CURVE ( 'NONE', #22180, #13955, #9180, .T. ) ;
#19183=EDGE_CURVE ( 'NONE', #13486, #2500, #7377, .T. ) ;
#19193=VERTEX_POINT ( 'NONE', #2425 ) ;
#19201=DIRECTION ( 'NONE',  ( -1.000000000000000000, -0.000000000000000000, -0.000000000000000000 ) ) ;
#19202=VERTEX_POINT ( 'NONE', #6516 ) ;
#19219=DIRECTION ( 'NONE',  ( -0.7071067811865364705, 8.659560562355067211E-17, -0.7071067811865584529 ) ) ;
#19273=LINE ( 'NONE', #17499, #17579 ) ;
#19303=SURFACE_STYLE_USAGE ( .BOTH. , #17300 ) ;
#19379=CIRCLE ( 'NONE', #2555, 2.500000000000000444 ) ;
#19415=VECTOR ( 'NONE', #10246, 1000.000000000000000 ) ;
#19439=FACE_OUTER_BOUND ( 'NONE', #4069, .T. ) ;
#19608=CARTESIAN_POINT ( 'NONE',  ( 4.999999999999997335, 5.204748896376250699E-16, -4.250000000000000000 ) ) ;
#19610=ADVANCED_FACE ( 'NONE', ( #1545 ), #8628, .F. ) ;
#19647=DIRECTION ( 'NONE',  ( 0.000000000000000000, 0.000000000000000000, 1.000000000000000000 ) ) ;
#19676=CARTESIAN_POINT ( 'NONE',  ( 20.55500000000001748, 0.000000000000000000, 0.000000000000000000 ) ) ;
#19727=CARTESIAN_POINT ( 'NONE',  ( 2.500000000000000000, 1.178949249685212974, -2.042000000000001148 ) ) ;
#19831=CARTESIAN_POINT ( 'NONE',  ( 0.000000000000000000, 0.000000000000000000, 0.000000000000000000 ) ) ;
#19954=CARTESIAN_POINT ( 'NONE',  ( 2.500000000000000000, 2.357898499370431722, -2.818925648462311528E-15 ) ) ;
#19977=EDGE_CURVE ( 'NONE', #13567, #15866, #10169, .T. ) ;
#19981=ORIENTED_EDGE ( 'NONE', *, *, #10441, .T. ) ;
#19986=DIRECTION ( 'NONE',  ( -1.000000000000000000, -0.000000000000000000, -0.000000000000000000 ) ) ;
#19998=DIRECTION ( 'NONE',  ( -1.000000000000000000, -0.000000000000000000, -0.000000000000000000 ) ) ;
#20011=DIRECTION ( 'NONE',  ( 1.000000000000000000, 0.000000000000000000, 0.000000000000000000 ) ) ;
#20023=LINE ( 'NONE', #10965, #6875 ) ;
#20038=ADVANCED_FACE ( 'NONE', ( #8827 ), #3636, .T. ) ;
#20065=EDGE_LOOP ( 'NONE', ( #7753, #3935, #13947, #9560 ) ) ;
#20119=ORIENTED_EDGE ( 'NONE', *, *, #4889, .T. ) ;
#20131=CARTESIAN_POINT ( 'NONE',  ( 21.00000000000000355, 0.000000000000000000, 0.000000000000000000 ) ) ;
#20213=DIRECTION ( 'NONE',  ( -1.000000000000000000, -0.000000000000000000, -0.000000000000000000 ) ) ;
#20224=AXIS2_PLACEMENT_3D ( 'NONE', #16898, #13547, #473 ) ;
#20300=SURFACE_STYLE_USAGE ( .BOTH. , #14835 ) ;
#20316=FACE_BOUND ( 'NONE', #7253, .T. ) ;
#20356=ORIENTED_EDGE ( 'NONE', *, *, #3635, .T. ) ;
#20416=DIRECTION ( 'NONE',  ( 0.000000000000000000, -0.5000000000000013323, -0.8660254037844380415 ) ) ;
#20439=DIRECTION ( 'NONE',  ( 0.000000000000000000, 0.000000000000000000, 1.000000000000000000 ) ) ;
#20447=FACE_OUTER_BOUND ( 'NONE', #8245, .T. ) ;
#20567=DIRECTION ( 'NONE',  ( -1.000000000000000000, -0.000000000000000000, -0.000000000000000000 ) ) ;
#20569=DIRECTION ( 'NONE',  ( -0.000000000000000000, 0.8660254037844392627, 0.4999999999999990008 ) ) ;
#20578=VECTOR ( 'NONE', #5064, 1000.000000000000000 ) ;
#20579=AXIS2_PLACEMENT_3D ( 'NONE', #2252, #20567, #7787 ) ;
#20615=VECTOR ( 'NONE', #2083, 1000.000000000000114 ) ;
#20628=ORIENTED_EDGE ( 'NONE', *, *, #12462, .F. ) ;
#20630=( NAMED_UNIT ( * ) PLANE_ANGLE_UNIT ( ) SI_UNIT ( $, .RADIAN. ) );
#20637=AXIS2_PLACEMENT_3D ( 'NONE', #12770, #17899, #16116 ) ;
#20646=AXIS2_PLACEMENT_3D ( 'NONE', #22145, #12970, #10824 ) ;
#20677=CARTESIAN_POINT ( 'NONE',  ( 5.000000000000000888, 0.000000000000000000, 0.000000000000000000 ) ) ;
#20699=ORIENTED_EDGE ( 'NONE', *, *, #9820, .F. ) ;
#20786=PRODUCT_DEFINITION_SHAPE ( 'NONE', 'NONE',  #10803 ) ;
#20830=CARTESIAN_POINT ( 'NONE',  ( 2.500000000000000000, 0.000000000000000000, 0.000000000000000000 ) ) ;
#20849=CARTESIAN_POINT ( 'NONE',  ( 0.000000000000000000, 2.357898499370431722, -2.818925648462311528E-15 ) ) ;
#20887=ORIENTED_EDGE ( 'NONE', *, *, #23627, .F. ) ;
#20936=FACE_OUTER_BOUND ( 'NONE', #4353, .T. ) ;
#20942=EDGE_LOOP ( 'NONE', ( #2608, #2347, #10087 ) ) ;
#20974=VECTOR ( 'NONE', #14532, 1000.000000000000114 ) ;
#20978=CONICAL_SURFACE ( 'NONE', #8773, 2.055000000000000160, 0.7853981633974639331 ) ;
#20984=PRODUCT_DEFINITION_FORMATION_WITH_SPECIFIED_SOURCE ( 'ANY', '', #908, .NOT_KNOWN. ) ;
#21009=ORIENTED_EDGE ( 'NONE', *, *, #479, .F. ) ;
#21032=VECTOR ( 'NONE', #22254, 1000.000000000000000 ) ;
#21046=DIRECTION ( 'NONE',  ( 0.000000000000000000, 0.000000000000000000, 1.000000000000000000 ) ) ;
#21062=CARTESIAN_POINT ( 'NONE',  ( 0.2500000000000002220, 0.000000000000000000, 4.250000000000000000 ) ) ;
#21085=CARTESIAN_POINT ( 'NONE',  ( 2.500000000000000000, 0.000000000000000000, 0.000000000000000000 ) ) ;
#21086=DIRECTION ( 'NONE',  ( -1.000000000000000000, -0.000000000000000000, -0.000000000000000000 ) ) ;
#21250=CARTESIAN_POINT ( 'NONE',  ( 2.500000000000000000, 1.178949249685212974, -2.042000000000001148 ) ) ;
#21300=COLOUR_RGB ( '', 0.09019608, 0.27058824, 0.51372549) ;
#21306=CARTESIAN_POINT ( 'NONE',  ( -31.74999999999995737, 0.000000000000000000, 0.000000000000000000 ) ) ;
#21322=( LENGTH_UNIT ( ) NAMED_UNIT ( * ) SI_UNIT ( .MILLI., .METRE. ) );
#21367=CIRCLE ( 'NONE', #336, 2.500000000000000444 ) ;
#21369=CIRCLE ( 'NONE', #6498, 2.700000000000000622 ) ;
#21380=ORIENTED_EDGE ( 'NONE', *, *, #2051, .T. ) ;
#21451=PLANE ( 'NONE',  #13352 ) ;
#21472=CARTESIAN_POINT ( 'NONE',  ( 2.500000000000000000, 2.357898499370431722, -2.818925648462311528E-15 ) ) ;
#21512=VECTOR ( 'NONE', #17520, 1000.000000000000114 ) ;
#21538=EDGE_LOOP ( 'NONE', ( #15965, #12312, #3473, #20119, #9647 ) ) ;
#21592=TOROIDAL_SURFACE ( 'NONE', #5161, 2.700000000000000622, 0.2000000000000000111 ) ;
#21600=ORIENTED_EDGE ( 'NONE', *, *, #22120, .T. ) ;
#21615=DIRECTION ( 'NONE',  ( 0.000000000000000000, 0.5000000000000009992, 0.8660254037844380415 ) ) ;
#21623=ORIENTED_EDGE ( 'NONE', *, *, #21636, .T. ) ;
#21636=EDGE_CURVE ( 'NONE', #7520, #19202, #18515, .T. ) ;
#21646=CARTESIAN_POINT ( 'NONE',  ( 0.2500000000000002220, 0.000000000000000000, 0.000000000000000000 ) ) ;
#21711=EDGE_LOOP ( 'NONE', ( #15933, #12077, #8794, #6425, #15970 ) ) ;
#21714=DIRECTION ( 'NONE',  ( -1.000000000000000000, -0.000000000000000000, -0.000000000000000000 ) ) ;
#21744=ORIENTED_EDGE ( 'NONE', *, *, #4343, .F. ) ;
#21806=CARTESIAN_POINT ( 'NONE',  ( 2.500000000000000000, 0.000000000000000000, 0.000000000000000000 ) ) ;
#21833=FACE_OUTER_BOUND ( 'NONE', #20942, .T. ) ;
#21845=DIRECTION ( 'NONE',  ( -1.000000000000000000, -0.000000000000000000, -0.000000000000000000 ) ) ;
#21979=DIRECTION ( 'NONE',  ( -0.5000000000000051070, 1.060575238724903217E-16, -0.8660254037844355990 ) ) ;
#21991=CARTESIAN_POINT ( 'NONE',  ( 5.000000000000002665, 0.000000000000000000, -2.700000000000000622 ) ) ;
#22120=EDGE_CURVE ( 'NONE', #13999, #13486, #13761, .T. ) ;
#22145=CARTESIAN_POINT ( 'NONE',  ( 2.500000000000000000, 0.000000000000000000, 0.000000000000000000 ) ) ;
#22161=AXIS2_PLACEMENT_3D ( 'NONE', #910, #23064, #15564 ) ;
#22162=ORIENTED_EDGE ( 'NONE', *, *, #16094, .T. ) ;
#22180=VERTEX_POINT ( 'NONE', #10233 ) ;
#22205=CARTESIAN_POINT ( 'NONE',  ( 2.500000000000000000, -1.768423874527825568, -1.020999999999998575 ) ) ;
#22215=CARTESIAN_POINT ( 'NONE',  ( 2.500000000000000000, 2.357898499370431722, -2.818925648462311528E-15 ) ) ;
#22254=DIRECTION ( 'NONE',  ( -1.000000000000000000, -0.000000000000000000, -0.000000000000000000 ) ) ;
#22268=CARTESIAN_POINT ( 'NONE',  ( 0.000000000000000000, -1.178949249685214307, 2.042000000000001592 ) ) ;
#22299=ORIENTED_EDGE ( 'NONE', *, *, #8339, .F. ) ;
#22347=DIRECTION ( 'NONE',  ( 0.000000000000000000, 0.000000000000000000, -1.000000000000000000 ) ) ;
#22372=FACE_OUTER_BOUND ( 'NONE', #15606, .T. ) ;
#22393=VECTOR ( 'NONE', #23098, 1000.000000000000114 ) ;
#22418=VERTEX_POINT ( 'NONE', #22205 ) ;
#22420=EDGE_LOOP ( 'NONE', ( #10969, #12914, #17733, #23261 ) ) ;
#22482=AXIS2_PLACEMENT_3D ( 'NONE', #20131, #18363, #9641 ) ;
#22485=PLANE ( 'NONE',  #2184 ) ;
#22526=EDGE_CURVE ( 'NONE', #15893, #10715, #13617, .T. ) ;
#22574=CARTESIAN_POINT ( 'NONE',  ( 2.500000000000000000, -1.178949249685214307, 2.042000000000001592 ) ) ;
#22588=ORIENTED_EDGE ( 'NONE', *, *, #5984, .F. ) ;
#22611=CARTESIAN_POINT ( 'NONE',  ( 5.200000000000002842, 0.000000000000000000, -2.700000000000000622 ) ) ;
#22635=DIRECTION ( 'NONE',  ( 0.000000000000000000, -0.4999999999999993339, 0.8660254037844390407 ) ) ;
#22639=ADVANCED_FACE ( 'NONE', ( #21833 ), #5435, .F. ) ;
#22648=EDGE_CURVE ( 'NONE', #10047, #22418, #20023, .T. ) ;
#22678=DIRECTION ( 'NONE',  ( -1.000000000000000000, -0.000000000000000000, -0.000000000000000000 ) ) ;
#22683=VECTOR ( 'NONE', #10229, 999.9999999999997726 ) ;
#22694=EDGE_CURVE ( 'NONE', #7612, #10715, #1506, .T. ) ;
#22717=EDGE_LOOP ( 'NONE', ( #12804, #9883 ) ) ;
#22753=DIRECTION ( 'NONE',  ( 0.000000000000000000, 0.000000000000000000, 1.000000000000000000 ) ) ;
#22758=ORIENTED_EDGE ( 'NONE', *, *, #13020, .T. ) ;
#22843=CARTESIAN_POINT ( 'NONE',  ( 2.500000000000000000, -1.178949249685218748, -2.041999999999998039 ) ) ;
#22901=ORIENTED_EDGE ( 'NONE', *, *, #23330, .T. ) ;
#22903=FILL_AREA_STYLE_COLOUR ( '', #7977 ) ;
#22931=EDGE_LOOP ( 'NONE', ( #4058, #10727, #5587 ) ) ;
#22997=VERTEX_POINT ( 'NONE', #15628 ) ;
#23029=FACE_OUTER_BOUND ( 'NONE', #16577, .T. ) ;
#23064=DIRECTION ( 'NONE',  ( 0.000000000000000000, -0.8660254037844390407, -0.4999999999999993339 ) ) ;
#23078=TOROIDAL_SURFACE ( 'NONE', #10106, 4.000000000000000000, 0.2500000000000000000 ) ;
#23096=ORIENTED_EDGE ( 'NONE', *, *, #6296, .F. ) ;
#23098=DIRECTION ( 'NONE',  ( 0.000000000000000000, 0.4999999999999990008, -0.8660254037844391517 ) ) ;
#23137=CARTESIAN_POINT ( 'NONE',  ( -31.74999999999995737, 5.204748896376250699E-16, -4.250000000000000000 ) ) ;
#23158=EDGE_CURVE ( 'NONE', #7520, #13999, #3251, .T. ) ;
#23163=DIRECTION ( 'NONE',  ( 1.000000000000000000, 0.000000000000000000, 0.000000000000000000 ) ) ;
#23253=ADVANCED_FACE ( 'NONE', ( #12633 ), #5364, .F. ) ;
#23261=ORIENTED_EDGE ( 'NONE', *, *, #5657, .F. ) ;
#23266=CARTESIAN_POINT ( 'NONE',  ( 5.200000000000002842, 3.061616997868383634E-16, -2.500000000000000444 ) ) ;
#23321=DIRECTION ( 'NONE',  ( 1.000000000000000000, 0.000000000000000000, 0.000000000000000000 ) ) ;
#23330=EDGE_CURVE ( 'NONE', #13955, #19202, #18343, .T. ) ;
#23405=DIRECTION ( 'NONE',  ( 0.000000000000000000, 0.000000000000000000, -1.000000000000000000 ) ) ;
#23418=CARTESIAN_POINT ( 'NONE',  ( 2.500000000000000000, -1.178949249685218748, -2.041999999999998039 ) ) ;
#23445=VERTEX_POINT ( 'NONE', #21062 ) ;
#23467=DIRECTION ( 'NONE',  ( -1.000000000000000000, -0.000000000000000000, -0.000000000000000000 ) ) ;
#23475=LINE ( 'NONE', #1908, #14189 ) ;
#23479=CARTESIAN_POINT ( 'NONE',  ( 2.500000000000000000, -1.178949249685214307, 2.042000000000001592 ) ) ;
#23498=CARTESIAN_POINT ( 'NONE',  ( 5.200000000000002842, 0.000000000000000000, 0.000000000000000000 ) ) ;
#23594=AXIS2_PLACEMENT_3D ( 'NONE', #269, #3872, #7376 ) ;
#23598=EDGE_CURVE ( 'NONE', #17065, #13999, #8464, .T. ) ;
#23627=EDGE_CURVE ( 'NONE', #13955, #8977, #19273, .T. ) ;
#23688=CARTESIAN_POINT ( 'NONE',  ( 0.000000000000000000, -1.178949249685214307, 2.042000000000001592 ) ) ;
ENDSEC;
END-ISO-10303-21;
